ISO-10303-21;
HEADER;
/* Generated by software containing ST-Developer
 * from STEP Tools, Inc. (www.steptools.com) 
 */

FILE_DESCRIPTION(
/* description */ ('Bin tilter linkage'),
/* implementation_level */ '2;1');

FILE_NAME(
/* name */ 'Pivot pin (2).step',
/* time_stamp */ '2026-10-28T03:26:24-07:00',
/* author */ (''),
/* organization */ (''),
/* preprocessor_version */ 'ST-DEVELOPER v20.2',
/* originating_system */ 'Autodesk Translation Framework v15.17.0.0',
/* authorisation */ '');

FILE_SCHEMA (('AUTOMOTIVE_DESIGN { 1 0 10303 214 3 1 1 }'));
ENDSEC;

DATA;
#10=MECHANICAL_DESIGN_GEOMETRIC_PRESENTATION_REPRESENTATION('',(#955),#23728);
#735=SHAPE_REPRESENTATION_RELATIONSHIP('SRR','None',#24203,#841);
#841=ADVANCED_BREP_SHAPE_REPRESENTATION('',(#1068),#23703);
#955=STYLED_ITEM('',(#24765),#1068);
#1068=MANIFOLD_SOLID_BREP('Body1',#12486);
#1428=FACE_BOUND('',#3634,.T.);
#1429=FACE_BOUND('',#3635,.T.);
#1430=FACE_BOUND('',#3636,.T.);
#1431=FACE_BOUND('',#3637,.T.);
#1432=FACE_BOUND('',#3639,.T.);
#1433=FACE_BOUND('',#3640,.T.);
#1434=FACE_BOUND('',#3641,.T.);
#1435=FACE_BOUND('',#3642,.T.);
#1436=FACE_BOUND('',#3648,.T.);
#1794=PLANE('',#15079);
#1795=PLANE('',#15089);
#1796=PLANE('',#15092);
#1797=PLANE('',#15100);
#1798=PLANE('',#15101);
#2510=FACE_OUTER_BOUND('',#3628,.T.);
#2511=FACE_OUTER_BOUND('',#3629,.T.);
#2512=FACE_OUTER_BOUND('',#3630,.T.);
#2513=FACE_OUTER_BOUND('',#3631,.T.);
#2514=FACE_OUTER_BOUND('',#3632,.T.);
#2515=FACE_OUTER_BOUND('',#3633,.T.);
#2516=FACE_OUTER_BOUND('',#3638,.T.);
#2517=FACE_OUTER_BOUND('',#3643,.T.);
#2518=FACE_OUTER_BOUND('',#3644,.T.);
#2519=FACE_OUTER_BOUND('',#3645,.T.);
#2520=FACE_OUTER_BOUND('',#3646,.T.);
#2521=FACE_OUTER_BOUND('',#3647,.T.);
#3628=EDGE_LOOP('',(#10687,#10688,#10689,#10690));
#3629=EDGE_LOOP('',(#10691));
#3630=EDGE_LOOP('',(#10692,#10693,#10694,#10695));
#3631=EDGE_LOOP('',(#10696,#10697,#10698,#10699));
#3632=EDGE_LOOP('',(#10700,#10701,#10702,#10703));
#3633=EDGE_LOOP('',(#10704));
#3634=EDGE_LOOP('',(#10705));
#3635=EDGE_LOOP('',(#10706));
#3636=EDGE_LOOP('',(#10707));
#3637=EDGE_LOOP('',(#10708));
#3638=EDGE_LOOP('',(#10709));
#3639=EDGE_LOOP('',(#10710));
#3640=EDGE_LOOP('',(#10711));
#3641=EDGE_LOOP('',(#10712));
#3642=EDGE_LOOP('',(#10713));
#3643=EDGE_LOOP('',(#10714,#10715,#10716,#10717));
#3644=EDGE_LOOP('',(#10718,#10719,#10720,#10721));
#3645=EDGE_LOOP('',(#10722,#10723,#10724,#10725));
#3646=EDGE_LOOP('',(#10726));
#3647=EDGE_LOOP('',(#10727));
#3648=EDGE_LOOP('',(#10728));
#4355=LINE('',#22741,#5030);
#4356=LINE('',#22748,#5031);
#4357=LINE('',#22754,#5032);
#4358=LINE('',#22760,#5033);
#4359=LINE('',#22773,#5034);
#4360=LINE('',#22776,#5035);
#4361=LINE('',#22781,#5036);
#5030=VECTOR('',#18784,0.164999999999999);
#5031=VECTOR('',#18793,0.225000000000001);
#5032=VECTOR('',#18800,0.225000000000001);
#5033=VECTOR('',#18807,0.225000000000001);
#5034=VECTOR('',#18824,1.5);
#5035=VECTOR('',#18827,0.600000000000001);
#5036=VECTOR('',#18834,0.600000000000001);
#5836=CIRCLE('',#15077,0.164999999999999);
#5837=CIRCLE('',#15078,0.164999999999999);
#5838=CIRCLE('',#15081,0.225000000000001);
#5839=CIRCLE('',#15082,0.225000000000001);
#5840=CIRCLE('',#15084,0.225000000000001);
#5841=CIRCLE('',#15085,0.225000000000001);
#5842=CIRCLE('',#15087,0.225000000000001);
#5843=CIRCLE('',#15088,0.225000000000001);
#5844=CIRCLE('',#15090,1.5);
#5845=CIRCLE('',#15091,0.600000000000001);
#5846=CIRCLE('',#15093,1.5);
#5847=CIRCLE('',#15094,0.600000000000001);
#5848=CIRCLE('',#15097,0.600000000000001);
#5849=CIRCLE('',#15099,0.600000000000001);
#6735=VERTEX_POINT('',#22738);
#6736=VERTEX_POINT('',#22740);
#6737=VERTEX_POINT('',#22745);
#6738=VERTEX_POINT('',#22747);
#6739=VERTEX_POINT('',#22751);
#6740=VERTEX_POINT('',#22753);
#6741=VERTEX_POINT('',#22757);
#6742=VERTEX_POINT('',#22759);
#6743=VERTEX_POINT('',#22763);
#6744=VERTEX_POINT('',#22765);
#6745=VERTEX_POINT('',#22768);
#6746=VERTEX_POINT('',#22770);
#6747=VERTEX_POINT('',#22775);
#6748=VERTEX_POINT('',#22779);
#8083=EDGE_CURVE('',#6735,#6735,#5836,.T.);
#8084=EDGE_CURVE('',#6735,#6736,#4355,.T.);
#8085=EDGE_CURVE('',#6736,#6736,#5837,.T.);
#8086=EDGE_CURVE('',#6737,#6737,#5838,.T.);
#8087=EDGE_CURVE('',#6737,#6738,#4356,.T.);
#8088=EDGE_CURVE('',#6738,#6738,#5839,.T.);
#8089=EDGE_CURVE('',#6739,#6739,#5840,.T.);
#8090=EDGE_CURVE('',#6739,#6740,#4357,.T.);
#8091=EDGE_CURVE('',#6740,#6740,#5841,.T.);
#8092=EDGE_CURVE('',#6741,#6741,#5842,.T.);
#8093=EDGE_CURVE('',#6741,#6742,#4358,.T.);
#8094=EDGE_CURVE('',#6742,#6742,#5843,.T.);
#8095=EDGE_CURVE('',#6743,#6743,#5844,.T.);
#8096=EDGE_CURVE('',#6744,#6744,#5845,.T.);
#8097=EDGE_CURVE('',#6745,#6745,#5846,.T.);
#8098=EDGE_CURVE('',#6746,#6746,#5847,.T.);
#8099=EDGE_CURVE('',#6743,#6745,#4359,.T.);
#8100=EDGE_CURVE('',#6746,#6747,#4360,.T.);
#8101=EDGE_CURVE('',#6747,#6747,#5848,.T.);
#8102=EDGE_CURVE('',#6748,#6748,#5849,.T.);
#8103=EDGE_CURVE('',#6748,#6744,#4361,.T.);
#10687=ORIENTED_EDGE('',*,*,#8083,.F.);
#10688=ORIENTED_EDGE('',*,*,#8084,.T.);
#10689=ORIENTED_EDGE('',*,*,#8085,.T.);
#10690=ORIENTED_EDGE('',*,*,#8084,.F.);
#10691=ORIENTED_EDGE('',*,*,#8085,.F.);
#10692=ORIENTED_EDGE('',*,*,#8086,.F.);
#10693=ORIENTED_EDGE('',*,*,#8087,.T.);
#10694=ORIENTED_EDGE('',*,*,#8088,.F.);
#10695=ORIENTED_EDGE('',*,*,#8087,.F.);
#10696=ORIENTED_EDGE('',*,*,#8089,.F.);
#10697=ORIENTED_EDGE('',*,*,#8090,.T.);
#10698=ORIENTED_EDGE('',*,*,#8091,.F.);
#10699=ORIENTED_EDGE('',*,*,#8090,.F.);
#10700=ORIENTED_EDGE('',*,*,#8092,.F.);
#10701=ORIENTED_EDGE('',*,*,#8093,.T.);
#10702=ORIENTED_EDGE('',*,*,#8094,.F.);
#10703=ORIENTED_EDGE('',*,*,#8093,.F.);
#10704=ORIENTED_EDGE('',*,*,#8095,.T.);
#10705=ORIENTED_EDGE('',*,*,#8088,.T.);
#10706=ORIENTED_EDGE('',*,*,#8091,.T.);
#10707=ORIENTED_EDGE('',*,*,#8094,.T.);
#10708=ORIENTED_EDGE('',*,*,#8096,.F.);
#10709=ORIENTED_EDGE('',*,*,#8097,.F.);
#10710=ORIENTED_EDGE('',*,*,#8086,.T.);
#10711=ORIENTED_EDGE('',*,*,#8089,.T.);
#10712=ORIENTED_EDGE('',*,*,#8092,.T.);
#10713=ORIENTED_EDGE('',*,*,#8098,.F.);
#10714=ORIENTED_EDGE('',*,*,#8095,.F.);
#10715=ORIENTED_EDGE('',*,*,#8099,.T.);
#10716=ORIENTED_EDGE('',*,*,#8097,.T.);
#10717=ORIENTED_EDGE('',*,*,#8099,.F.);
#10718=ORIENTED_EDGE('',*,*,#8098,.T.);
#10719=ORIENTED_EDGE('',*,*,#8100,.T.);
#10720=ORIENTED_EDGE('',*,*,#8101,.T.);
#10721=ORIENTED_EDGE('',*,*,#8100,.F.);
#10722=ORIENTED_EDGE('',*,*,#8102,.F.);
#10723=ORIENTED_EDGE('',*,*,#8103,.T.);
#10724=ORIENTED_EDGE('',*,*,#8096,.T.);
#10725=ORIENTED_EDGE('',*,*,#8103,.F.);
#10726=ORIENTED_EDGE('',*,*,#8102,.T.);
#10727=ORIENTED_EDGE('',*,*,#8101,.F.);
#10728=ORIENTED_EDGE('',*,*,#8083,.T.);
#11561=CYLINDRICAL_SURFACE('',#15076,0.164999999999999);
#11562=CYLINDRICAL_SURFACE('',#15080,0.225000000000001);
#11563=CYLINDRICAL_SURFACE('',#15083,0.225000000000001);
#11564=CYLINDRICAL_SURFACE('',#15086,0.225000000000001);
#11565=CYLINDRICAL_SURFACE('',#15095,1.5);
#11566=CYLINDRICAL_SURFACE('',#15096,0.600000000000001);
#11567=CYLINDRICAL_SURFACE('',#15098,0.600000000000001);
#12235=ADVANCED_FACE('',(#2510),#11561,.F.);
#12236=ADVANCED_FACE('',(#2511),#1794,.F.);
#12237=ADVANCED_FACE('',(#2512),#11562,.F.);
#12238=ADVANCED_FACE('',(#2513),#11563,.F.);
#12239=ADVANCED_FACE('',(#2514),#11564,.F.);
#12240=ADVANCED_FACE('',(#2515,#1428,#1429,#1430,#1431),#1795,.T.);
#12241=ADVANCED_FACE('',(#2516,#1432,#1433,#1434,#1435),#1796,.F.);
#12242=ADVANCED_FACE('',(#2517),#11565,.T.);
#12243=ADVANCED_FACE('',(#2518),#11566,.T.);
#12244=ADVANCED_FACE('',(#2519),#11567,.T.);
#12245=ADVANCED_FACE('',(#2520),#1797,.T.);
#12246=ADVANCED_FACE('',(#2521,#1436),#1798,.F.);
#12486=CLOSED_SHELL('',(#12235,#12236,#12237,#12238,#12239,#12240,#12241,
#12242,#12243,#12244,#12245,#12246));
#15075=AXIS2_PLACEMENT_3D('',#22736,#18778,#18779);
#15076=AXIS2_PLACEMENT_3D('',#22737,#18780,#18781);
#15077=AXIS2_PLACEMENT_3D('',#22739,#18782,#18783);
#15078=AXIS2_PLACEMENT_3D('',#22742,#18785,#18786);
#15079=AXIS2_PLACEMENT_3D('',#22743,#18787,#18788);
#15080=AXIS2_PLACEMENT_3D('',#22744,#18789,#18790);
#15081=AXIS2_PLACEMENT_3D('',#22746,#18791,#18792);
#15082=AXIS2_PLACEMENT_3D('',#22749,#18794,#18795);
#15083=AXIS2_PLACEMENT_3D('',#22750,#18796,#18797);
#15084=AXIS2_PLACEMENT_3D('',#22752,#18798,#18799);
#15085=AXIS2_PLACEMENT_3D('',#22755,#18801,#18802);
#15086=AXIS2_PLACEMENT_3D('',#22756,#18803,#18804);
#15087=AXIS2_PLACEMENT_3D('',#22758,#18805,#18806);
#15088=AXIS2_PLACEMENT_3D('',#22761,#18808,#18809);
#15089=AXIS2_PLACEMENT_3D('',#22762,#18810,#18811);
#15090=AXIS2_PLACEMENT_3D('',#22764,#18812,#18813);
#15091=AXIS2_PLACEMENT_3D('',#22766,#18814,#18815);
#15092=AXIS2_PLACEMENT_3D('',#22767,#18816,#18817);
#15093=AXIS2_PLACEMENT_3D('',#22769,#18818,#18819);
#15094=AXIS2_PLACEMENT_3D('',#22771,#18820,#18821);
#15095=AXIS2_PLACEMENT_3D('',#22772,#18822,#18823);
#15096=AXIS2_PLACEMENT_3D('',#22774,#18825,#18826);
#15097=AXIS2_PLACEMENT_3D('',#22777,#18828,#18829);
#15098=AXIS2_PLACEMENT_3D('',#22778,#18830,#18831);
#15099=AXIS2_PLACEMENT_3D('',#22780,#18832,#18833);
#15100=AXIS2_PLACEMENT_3D('',#22782,#18835,#18836);
#15101=AXIS2_PLACEMENT_3D('',#22783,#18837,#18838);
#18778=DIRECTION('axis',(0.,0.,1.));
#18779=DIRECTION('refdir',(1.,0.,0.));
#18780=DIRECTION('center_axis',(0.,1.,0.));
#18781=DIRECTION('ref_axis',(1.,0.,0.));
#18782=DIRECTION('center_axis',(0.,1.,0.));
#18783=DIRECTION('ref_axis',(1.,0.,0.));
#18784=DIRECTION('',(0.,1.,0.));
#18785=DIRECTION('center_axis',(0.,1.,0.));
#18786=DIRECTION('ref_axis',(1.,0.,0.));
#18787=DIRECTION('center_axis',(0.,1.,0.));
#18788=DIRECTION('ref_axis',(1.,0.,0.));
#18789=DIRECTION('center_axis',(0.,1.,0.));
#18790=DIRECTION('ref_axis',(1.,0.,0.));
#18791=DIRECTION('center_axis',(0.,1.,0.));
#18792=DIRECTION('ref_axis',(1.,0.,0.));
#18793=DIRECTION('',(0.,1.,0.));
#18794=DIRECTION('center_axis',(0.,-1.,0.));
#18795=DIRECTION('ref_axis',(1.,0.,0.));
#18796=DIRECTION('center_axis',(0.,1.,0.));
#18797=DIRECTION('ref_axis',(1.,0.,0.));
#18798=DIRECTION('center_axis',(0.,1.,0.));
#18799=DIRECTION('ref_axis',(1.,0.,0.));
#18800=DIRECTION('',(0.,1.,0.));
#18801=DIRECTION('center_axis',(0.,-1.,0.));
#18802=DIRECTION('ref_axis',(1.,0.,0.));
#18803=DIRECTION('center_axis',(0.,1.,0.));
#18804=DIRECTION('ref_axis',(1.,0.,0.));
#18805=DIRECTION('center_axis',(0.,1.,0.));
#18806=DIRECTION('ref_axis',(1.,0.,0.));
#18807=DIRECTION('',(0.,1.,0.));
#18808=DIRECTION('center_axis',(0.,-1.,0.));
#18809=DIRECTION('ref_axis',(1.,0.,0.));
#18810=DIRECTION('center_axis',(0.,1.,0.));
#18811=DIRECTION('ref_axis',(1.,0.,0.));
#18812=DIRECTION('center_axis',(0.,1.,0.));
#18813=DIRECTION('ref_axis',(1.,0.,0.));
#18814=DIRECTION('center_axis',(0.,1.,0.));
#18815=DIRECTION('ref_axis',(1.,0.,0.));
#18816=DIRECTION('center_axis',(0.,1.,0.));
#18817=DIRECTION('ref_axis',(1.,0.,0.));
#18818=DIRECTION('center_axis',(0.,1.,0.));
#18819=DIRECTION('ref_axis',(1.,0.,0.));
#18820=DIRECTION('center_axis',(0.,-1.,0.));
#18821=DIRECTION('ref_axis',(1.,0.,0.));
#18822=DIRECTION('center_axis',(0.,1.,0.));
#18823=DIRECTION('ref_axis',(1.,0.,0.));
#18824=DIRECTION('',(0.,-1.,0.));
#18825=DIRECTION('center_axis',(0.,1.,0.));
#18826=DIRECTION('ref_axis',(1.,0.,0.));
#18827=DIRECTION('',(0.,-1.,0.));
#18828=DIRECTION('center_axis',(0.,1.,0.));
#18829=DIRECTION('ref_axis',(1.,0.,0.));
#18830=DIRECTION('center_axis',(0.,1.,0.));
#18831=DIRECTION('ref_axis',(1.,0.,0.));
#18832=DIRECTION('center_axis',(0.,1.,0.));
#18833=DIRECTION('ref_axis',(1.,0.,0.));
#18834=DIRECTION('',(0.,-1.,0.));
#18835=DIRECTION('center_axis',(0.,1.,0.));
#18836=DIRECTION('ref_axis',(1.,0.,0.));
#18837=DIRECTION('center_axis',(0.,1.,0.));
#18838=DIRECTION('ref_axis',(1.,0.,0.));
#22736=CARTESIAN_POINT('',(0.,0.,0.));
#22737=CARTESIAN_POINT('Origin',(24.2020784790221,-1.1,28.6577532024872));
#22738=CARTESIAN_POINT('',(24.0370784790221,-1.,28.6577532024872));
#22739=CARTESIAN_POINT('Origin',(24.2020784790221,-1.,28.6577532024872));
#22740=CARTESIAN_POINT('',(24.0370784790221,0.6,28.6577532024872));
#22741=CARTESIAN_POINT('',(24.0370784790221,-1.1,28.6577532024872));
#22742=CARTESIAN_POINT('Origin',(24.2020784790221,0.6,28.6577532024872));
#22743=CARTESIAN_POINT('Origin',(24.2020784790221,0.6,28.6577532024872));
#22744=CARTESIAN_POINT('Origin',(25.3520784790221,2.,28.6577532024872));
#22745=CARTESIAN_POINT('',(25.1270784790221,2.1,28.6577532024872));
#22746=CARTESIAN_POINT('Origin',(25.3520784790221,2.1,28.6577532024872));
#22747=CARTESIAN_POINT('',(25.1270784790221,2.5,28.6577532024872));
#22748=CARTESIAN_POINT('',(25.1270784790221,2.,28.6577532024872));
#22749=CARTESIAN_POINT('Origin',(25.3520784790221,2.5,28.6577532024872));
#22750=CARTESIAN_POINT('Origin',(23.6270784790221,2.,29.6536824168393));
#22751=CARTESIAN_POINT('',(23.4020784790221,2.1,29.6536824168393));
#22752=CARTESIAN_POINT('Origin',(23.6270784790221,2.1,29.6536824168393));
#22753=CARTESIAN_POINT('',(23.4020784790221,2.5,29.6536824168393));
#22754=CARTESIAN_POINT('',(23.4020784790221,2.,29.6536824168393));
#22755=CARTESIAN_POINT('Origin',(23.6270784790221,2.5,29.6536824168393));
#22756=CARTESIAN_POINT('Origin',(23.6270784790221,2.,27.6618239881351));
#22757=CARTESIAN_POINT('',(23.4020784790221,2.1,27.6618239881351));
#22758=CARTESIAN_POINT('Origin',(23.6270784790221,2.1,27.6618239881351));
#22759=CARTESIAN_POINT('',(23.4020784790221,2.5,27.6618239881351));
#22760=CARTESIAN_POINT('',(23.4020784790221,2.,27.6618239881351));
#22761=CARTESIAN_POINT('Origin',(23.6270784790221,2.5,27.6618239881351));
#22762=CARTESIAN_POINT('Origin',(24.2020784790221,2.5,28.6577532024872));
#22763=CARTESIAN_POINT('',(22.7020784790221,2.5,28.6577532024872));
#22764=CARTESIAN_POINT('Origin',(24.2020784790221,2.5,28.6577532024872));
#22765=CARTESIAN_POINT('',(23.6020784790221,2.5,28.6577532024872));
#22766=CARTESIAN_POINT('Origin',(24.2020784790221,2.5,28.6577532024872));
#22767=CARTESIAN_POINT('Origin',(24.2020784790221,2.1,28.6577532024872));
#22768=CARTESIAN_POINT('',(22.7020784790221,2.1,28.6577532024872));
#22769=CARTESIAN_POINT('Origin',(24.2020784790221,2.1,28.6577532024872));
#22770=CARTESIAN_POINT('',(23.6020784790221,2.1,28.6577532024872));
#22771=CARTESIAN_POINT('Origin',(24.2020784790221,2.1,28.6577532024872));
#22772=CARTESIAN_POINT('Origin',(24.2020784790221,2.1,28.6577532024872));
#22773=CARTESIAN_POINT('',(22.7020784790221,2.1,28.6577532024872));
#22774=CARTESIAN_POINT('Origin',(24.2020784790221,-1.,28.6577532024872));
#22775=CARTESIAN_POINT('',(23.6020784790221,-1.,28.6577532024872));
#22776=CARTESIAN_POINT('',(23.6020784790221,-1.,28.6577532024872));
#22777=CARTESIAN_POINT('Origin',(24.2020784790221,-1.,28.6577532024872));
#22778=CARTESIAN_POINT('Origin',(24.2020784790221,-1.,28.6577532024872));
#22779=CARTESIAN_POINT('',(23.6020784790221,3.5,28.6577532024872));
#22780=CARTESIAN_POINT('Origin',(24.2020784790221,3.5,28.6577532024872));
#22781=CARTESIAN_POINT('',(23.6020784790221,-1.,28.6577532024872));
#22782=CARTESIAN_POINT('Origin',(24.2020784790221,3.5,28.6577532024872));
#22783=CARTESIAN_POINT('Origin',(24.2020784790221,-1.,28.6577532024872));
#23586=UNCERTAINTY_MEASURE_WITH_UNIT(LENGTH_MEASURE(0.001),#23729,
'DISTANCE_ACCURACY_VALUE',
'Maximum model space distance between geometric entities at asserted c
onnectivities');
#23611=UNCERTAINTY_MEASURE_WITH_UNIT(LENGTH_MEASURE(0.001),#23729,
'DISTANCE_ACCURACY_VALUE',
'Maximum model space distance between geometric entities at asserted c
onnectivities');
#23703=(
GEOMETRIC_REPRESENTATION_CONTEXT(3)
GLOBAL_UNCERTAINTY_ASSIGNED_CONTEXT((#23586))
GLOBAL_UNIT_ASSIGNED_CONTEXT((#23729,#23731,#23732))
REPRESENTATION_CONTEXT('','3D')
);
#23728=(
GEOMETRIC_REPRESENTATION_CONTEXT(3)
GLOBAL_UNCERTAINTY_ASSIGNED_CONTEXT((#23611))
GLOBAL_UNIT_ASSIGNED_CONTEXT((#23729,#23731,#23732))
REPRESENTATION_CONTEXT('','3D')
);
#23729=(
LENGTH_UNIT()
NAMED_UNIT(*)
SI_UNIT(.CENTI.,.METRE.)
);
#23731=(
NAMED_UNIT(*)
PLANE_ANGLE_UNIT()
SI_UNIT($,.RADIAN.)
);
#23732=(
NAMED_UNIT(*)
SI_UNIT($,.STERADIAN.)
SOLID_ANGLE_UNIT()
);
#23824=SHAPE_DEFINITION_REPRESENTATION(#23991,#24203);
#23991=PRODUCT_DEFINITION_SHAPE('',$,#24320);
#24203=SHAPE_REPRESENTATION('',(#15075),#23703);
#24228=PRODUCT_DEFINITION_CONTEXT('part definition',#24578,'design');
#24320=PRODUCT_DEFINITION('Pivot pin (2)','Pivot pin (2)',#24436,#24228);
#24436=PRODUCT_DEFINITION_FORMATION('',$,#24671);
#24578=APPLICATION_CONTEXT(
'Core Data for Automotive Mechanical Design Process');
#24579=PRODUCT_CONTEXT('part definition',#24578,'mechanical');
#24671=PRODUCT('Pivot pin (2)','Pivot pin (2)','Pivot pin (2)',(#24579));
#24759=COLOUR_RGB('Grey',0.48,0.52,0.57);
#24760=FILL_AREA_STYLE_COLOUR('',#24759);
#24761=FILL_AREA_STYLE('',(#24760));
#24762=SURFACE_STYLE_FILL_AREA(#24761);
#24763=SURFACE_SIDE_STYLE('',(#24762));
#24764=SURFACE_STYLE_USAGE(.BOTH.,#24763);
#24765=PRESENTATION_STYLE_ASSIGNMENT((#24764));
ENDSEC;
END-ISO-10303-21;
